ISO-10303-21;
HEADER;
/* Generated by software containing ST-Developer
 * from STEP Tools, Inc. (www.steptools.com) 
 */

FILE_DESCRIPTION(
/* description */ ('Bell-crank linkage with push rods'),
/* implementation_level */ '2;1');

FILE_NAME(
/* name */ 'Horizontal link pin (1).step',
/* time_stamp */ '2026-10-28T03:25:15-07:00',
/* author */ (''),
/* organization */ (''),
/* preprocessor_version */ 'ST-DEVELOPER v20.2',
/* originating_system */ 'Autodesk Translation Framework v15.17.0.0',
/* authorisation */ '');

FILE_SCHEMA (('AUTOMOTIVE_DESIGN { 1 0 10303 214 3 1 1 }'));
ENDSEC;

DATA;
#10=MECHANICAL_DESIGN_GEOMETRIC_PRESENTATION_REPRESENTATION('',(#652),#16678);
#536=SHAPE_REPRESENTATION_RELATIONSHIP('SRR','None',#16957,#590);
#590=ADVANCED_BREP_SHAPE_REPRESENTATION('',(#712),#16662);
#652=STYLED_ITEM('',(#17291),#712);
#712=MANIFOLD_SOLID_BREP('Body1',#8844);
#905=FACE_BOUND('',#2356,.T.);
#906=FACE_BOUND('',#2358,.T.);
#907=FACE_BOUND('',#2363,.T.);
#1178=PLANE('',#10309);
#1179=PLANE('',#10310);
#1180=PLANE('',#10313);
#1181=PLANE('',#10321);
#1182=PLANE('',#10322);
#1651=FACE_OUTER_BOUND('',#2353,.T.);
#1652=FACE_OUTER_BOUND('',#2354,.T.);
#1653=FACE_OUTER_BOUND('',#2355,.T.);
#1654=FACE_OUTER_BOUND('',#2357,.T.);
#1655=FACE_OUTER_BOUND('',#2359,.T.);
#1656=FACE_OUTER_BOUND('',#2360,.T.);
#1657=FACE_OUTER_BOUND('',#2361,.T.);
#1658=FACE_OUTER_BOUND('',#2362,.T.);
#1659=FACE_OUTER_BOUND('',#2364,.T.);
#2353=EDGE_LOOP('',(#7623,#7624,#7625,#7626));
#2354=EDGE_LOOP('',(#7627));
#2355=EDGE_LOOP('',(#7628));
#2356=EDGE_LOOP('',(#7629));
#2357=EDGE_LOOP('',(#7630));
#2358=EDGE_LOOP('',(#7631));
#2359=EDGE_LOOP('',(#7632,#7633,#7634,#7635));
#2360=EDGE_LOOP('',(#7636,#7637,#7638,#7639));
#2361=EDGE_LOOP('',(#7640,#7641,#7642,#7643));
#2362=EDGE_LOOP('',(#7644));
#2363=EDGE_LOOP('',(#7645));
#2364=EDGE_LOOP('',(#7646));
#2960=LINE('',#15963,#3509);
#2961=LINE('',#15977,#3510);
#2962=LINE('',#15980,#3511);
#2963=LINE('',#15985,#3512);
#3509=VECTOR('',#12766,0.164999999999999);
#3510=VECTOR('',#12785,0.699999999999999);
#3511=VECTOR('',#12788,0.300000000000001);
#3512=VECTOR('',#12795,0.300000000000001);
#4019=CIRCLE('',#10307,0.164999999999999);
#4020=CIRCLE('',#10308,0.164999999999999);
#4021=CIRCLE('',#10311,0.699999999999999);
#4022=CIRCLE('',#10312,0.300000000000001);
#4023=CIRCLE('',#10314,0.699999999999999);
#4024=CIRCLE('',#10315,0.300000000000001);
#4025=CIRCLE('',#10318,0.300000000000001);
#4026=CIRCLE('',#10320,0.300000000000001);
#4686=VERTEX_POINT('',#15960);
#4687=VERTEX_POINT('',#15962);
#4688=VERTEX_POINT('',#15967);
#4689=VERTEX_POINT('',#15969);
#4690=VERTEX_POINT('',#15972);
#4691=VERTEX_POINT('',#15974);
#4692=VERTEX_POINT('',#15979);
#4693=VERTEX_POINT('',#15983);
#5689=EDGE_CURVE('',#4686,#4686,#4019,.T.);
#5690=EDGE_CURVE('',#4686,#4687,#2960,.T.);
#5691=EDGE_CURVE('',#4687,#4687,#4020,.T.);
#5692=EDGE_CURVE('',#4688,#4688,#4021,.T.);
#5693=EDGE_CURVE('',#4689,#4689,#4022,.T.);
#5694=EDGE_CURVE('',#4690,#4690,#4023,.T.);
#5695=EDGE_CURVE('',#4691,#4691,#4024,.T.);
#5696=EDGE_CURVE('',#4688,#4690,#2961,.T.);
#5697=EDGE_CURVE('',#4691,#4692,#2962,.T.);
#5698=EDGE_CURVE('',#4692,#4692,#4025,.T.);
#5699=EDGE_CURVE('',#4693,#4693,#4026,.T.);
#5700=EDGE_CURVE('',#4693,#4689,#2963,.T.);
#7623=ORIENTED_EDGE('',*,*,#5689,.F.);
#7624=ORIENTED_EDGE('',*,*,#5690,.T.);
#7625=ORIENTED_EDGE('',*,*,#5691,.F.);
#7626=ORIENTED_EDGE('',*,*,#5690,.F.);
#7627=ORIENTED_EDGE('',*,*,#5689,.T.);
#7628=ORIENTED_EDGE('',*,*,#5692,.T.);
#7629=ORIENTED_EDGE('',*,*,#5693,.F.);
#7630=ORIENTED_EDGE('',*,*,#5694,.F.);
#7631=ORIENTED_EDGE('',*,*,#5695,.F.);
#7632=ORIENTED_EDGE('',*,*,#5692,.F.);
#7633=ORIENTED_EDGE('',*,*,#5696,.T.);
#7634=ORIENTED_EDGE('',*,*,#5694,.T.);
#7635=ORIENTED_EDGE('',*,*,#5696,.F.);
#7636=ORIENTED_EDGE('',*,*,#5695,.T.);
#7637=ORIENTED_EDGE('',*,*,#5697,.T.);
#7638=ORIENTED_EDGE('',*,*,#5698,.T.);
#7639=ORIENTED_EDGE('',*,*,#5697,.F.);
#7640=ORIENTED_EDGE('',*,*,#5699,.F.);
#7641=ORIENTED_EDGE('',*,*,#5700,.T.);
#7642=ORIENTED_EDGE('',*,*,#5693,.T.);
#7643=ORIENTED_EDGE('',*,*,#5700,.F.);
#7644=ORIENTED_EDGE('',*,*,#5699,.T.);
#7645=ORIENTED_EDGE('',*,*,#5691,.T.);
#7646=ORIENTED_EDGE('',*,*,#5698,.F.);
#8226=CYLINDRICAL_SURFACE('',#10306,0.164999999999999);
#8227=CYLINDRICAL_SURFACE('',#10316,0.699999999999999);
#8228=CYLINDRICAL_SURFACE('',#10317,0.300000000000001);
#8229=CYLINDRICAL_SURFACE('',#10319,0.300000000000001);
#8676=ADVANCED_FACE('',(#1651),#8226,.F.);
#8677=ADVANCED_FACE('',(#1652),#1178,.T.);
#8678=ADVANCED_FACE('',(#1653,#905),#1179,.T.);
#8679=ADVANCED_FACE('',(#1654,#906),#1180,.F.);
#8680=ADVANCED_FACE('',(#1655),#8227,.T.);
#8681=ADVANCED_FACE('',(#1656),#8228,.T.);
#8682=ADVANCED_FACE('',(#1657),#8229,.T.);
#8683=ADVANCED_FACE('',(#1658,#907),#1181,.T.);
#8684=ADVANCED_FACE('',(#1659),#1182,.F.);
#8844=CLOSED_SHELL('',(#8676,#8677,#8678,#8679,#8680,#8681,#8682,#8683,
#8684));
#10305=AXIS2_PLACEMENT_3D('',#15958,#12760,#12761);
#10306=AXIS2_PLACEMENT_3D('',#15959,#12762,#12763);
#10307=AXIS2_PLACEMENT_3D('',#15961,#12764,#12765);
#10308=AXIS2_PLACEMENT_3D('',#15964,#12767,#12768);
#10309=AXIS2_PLACEMENT_3D('',#15965,#12769,#12770);
#10310=AXIS2_PLACEMENT_3D('',#15966,#12771,#12772);
#10311=AXIS2_PLACEMENT_3D('',#15968,#12773,#12774);
#10312=AXIS2_PLACEMENT_3D('',#15970,#12775,#12776);
#10313=AXIS2_PLACEMENT_3D('',#15971,#12777,#12778);
#10314=AXIS2_PLACEMENT_3D('',#15973,#12779,#12780);
#10315=AXIS2_PLACEMENT_3D('',#15975,#12781,#12782);
#10316=AXIS2_PLACEMENT_3D('',#15976,#12783,#12784);
#10317=AXIS2_PLACEMENT_3D('',#15978,#12786,#12787);
#10318=AXIS2_PLACEMENT_3D('',#15981,#12789,#12790);
#10319=AXIS2_PLACEMENT_3D('',#15982,#12791,#12792);
#10320=AXIS2_PLACEMENT_3D('',#15984,#12793,#12794);
#10321=AXIS2_PLACEMENT_3D('',#15986,#12796,#12797);
#10322=AXIS2_PLACEMENT_3D('',#15987,#12798,#12799);
#12760=DIRECTION('axis',(0.,0.,1.));
#12761=DIRECTION('refdir',(1.,0.,0.));
#12762=DIRECTION('center_axis',(0.,0.,1.));
#12763=DIRECTION('ref_axis',(1.,0.,0.));
#12764=DIRECTION('center_axis',(0.,0.,1.));
#12765=DIRECTION('ref_axis',(1.,0.,0.));
#12766=DIRECTION('',(0.,0.,1.));
#12767=DIRECTION('center_axis',(0.,0.,-1.));
#12768=DIRECTION('ref_axis',(1.,0.,0.));
#12769=DIRECTION('center_axis',(0.,0.,1.));
#12770=DIRECTION('ref_axis',(1.,0.,0.));
#12771=DIRECTION('center_axis',(0.,0.,1.));
#12772=DIRECTION('ref_axis',(1.,0.,0.));
#12773=DIRECTION('center_axis',(0.,0.,1.));
#12774=DIRECTION('ref_axis',(1.,0.,0.));
#12775=DIRECTION('center_axis',(0.,0.,1.));
#12776=DIRECTION('ref_axis',(1.,0.,0.));
#12777=DIRECTION('center_axis',(0.,0.,1.));
#12778=DIRECTION('ref_axis',(1.,0.,0.));
#12779=DIRECTION('center_axis',(0.,0.,1.));
#12780=DIRECTION('ref_axis',(1.,0.,0.));
#12781=DIRECTION('center_axis',(0.,0.,-1.));
#12782=DIRECTION('ref_axis',(1.,0.,0.));
#12783=DIRECTION('center_axis',(0.,0.,1.));
#12784=DIRECTION('ref_axis',(1.,0.,0.));
#12785=DIRECTION('',(0.,0.,-1.));
#12786=DIRECTION('center_axis',(0.,0.,1.));
#12787=DIRECTION('ref_axis',(1.,0.,0.));
#12788=DIRECTION('',(0.,0.,-1.));
#12789=DIRECTION('center_axis',(0.,0.,1.));
#12790=DIRECTION('ref_axis',(1.,0.,0.));
#12791=DIRECTION('center_axis',(0.,0.,1.));
#12792=DIRECTION('ref_axis',(1.,0.,0.));
#12793=DIRECTION('center_axis',(0.,0.,1.));
#12794=DIRECTION('ref_axis',(1.,0.,0.));
#12795=DIRECTION('',(0.,0.,-1.));
#12796=DIRECTION('center_axis',(0.,0.,1.));
#12797=DIRECTION('ref_axis',(1.,0.,0.));
#12798=DIRECTION('center_axis',(0.,0.,1.));
#12799=DIRECTION('ref_axis',(1.,0.,0.));
#15958=CARTESIAN_POINT('',(0.,0.,0.));
#15959=CARTESIAN_POINT('Origin',(10.,2.,9.1));
#15960=CARTESIAN_POINT('',(9.835,2.,9.1));
#15961=CARTESIAN_POINT('Origin',(10.,2.,9.1));
#15962=CARTESIAN_POINT('',(9.835,2.,10.1));
#15963=CARTESIAN_POINT('',(9.835,2.,9.1));
#15964=CARTESIAN_POINT('Origin',(10.,2.,10.1));
#15965=CARTESIAN_POINT('Origin',(10.,2.,9.1));
#15966=CARTESIAN_POINT('Origin',(10.,2.,6.1));
#15967=CARTESIAN_POINT('',(9.3,2.,6.1));
#15968=CARTESIAN_POINT('Origin',(10.,2.,6.1));
#15969=CARTESIAN_POINT('',(9.7,2.,6.1));
#15970=CARTESIAN_POINT('Origin',(10.,2.,6.1));
#15971=CARTESIAN_POINT('Origin',(10.,2.,5.7));
#15972=CARTESIAN_POINT('',(9.3,2.,5.7));
#15973=CARTESIAN_POINT('Origin',(10.,2.,5.7));
#15974=CARTESIAN_POINT('',(9.7,2.,5.7));
#15975=CARTESIAN_POINT('Origin',(10.,2.,5.7));
#15976=CARTESIAN_POINT('Origin',(10.,2.,5.7));
#15977=CARTESIAN_POINT('',(9.3,2.,5.7));
#15978=CARTESIAN_POINT('Origin',(10.,2.,5.2));
#15979=CARTESIAN_POINT('',(9.7,2.,5.2));
#15980=CARTESIAN_POINT('',(9.7,2.,5.2));
#15981=CARTESIAN_POINT('Origin',(10.,2.,5.2));
#15982=CARTESIAN_POINT('Origin',(10.,2.,5.2));
#15983=CARTESIAN_POINT('',(9.7,2.,10.1));
#15984=CARTESIAN_POINT('Origin',(10.,2.,10.1));
#15985=CARTESIAN_POINT('',(9.7,2.,5.2));
#15986=CARTESIAN_POINT('Origin',(10.,2.,10.1));
#15987=CARTESIAN_POINT('Origin',(10.,2.,5.2));
#16598=UNCERTAINTY_MEASURE_WITH_UNIT(LENGTH_MEASURE(0.001),#16679,
'DISTANCE_ACCURACY_VALUE',
'Maximum model space distance between geometric entities at asserted c
onnectivities');
#16614=UNCERTAINTY_MEASURE_WITH_UNIT(LENGTH_MEASURE(0.001),#16679,
'DISTANCE_ACCURACY_VALUE',
'Maximum model space distance between geometric entities at asserted c
onnectivities');
#16662=(
GEOMETRIC_REPRESENTATION_CONTEXT(3)
GLOBAL_UNCERTAINTY_ASSIGNED_CONTEXT((#16598))
GLOBAL_UNIT_ASSIGNED_CONTEXT((#16679,#16681,#16682))
REPRESENTATION_CONTEXT('','3D')
);
#16678=(
GEOMETRIC_REPRESENTATION_CONTEXT(3)
GLOBAL_UNCERTAINTY_ASSIGNED_CONTEXT((#16614))
GLOBAL_UNIT_ASSIGNED_CONTEXT((#16679,#16681,#16682))
REPRESENTATION_CONTEXT('','3D')
);
#16679=(
LENGTH_UNIT()
NAMED_UNIT(*)
SI_UNIT(.CENTI.,.METRE.)
);
#16681=(
NAMED_UNIT(*)
PLANE_ANGLE_UNIT()
SI_UNIT($,.RADIAN.)
);
#16682=(
NAMED_UNIT(*)
SI_UNIT($,.STERADIAN.)
SOLID_ANGLE_UNIT()
);
#16730=SHAPE_DEFINITION_REPRESENTATION(#16804,#16957);
#16804=PRODUCT_DEFINITION_SHAPE('',$,#17021);
#16957=SHAPE_REPRESENTATION('',(#10305),#16662);
#16973=PRODUCT_DEFINITION_CONTEXT('part definition',#17164,'design');
#17021=PRODUCT_DEFINITION('Horizontal link pin (1)',
'Horizontal link pin (1)',#17084,#16973);
#17084=PRODUCT_DEFINITION_FORMATION('',$,#17213);
#17164=APPLICATION_CONTEXT(
'Core Data for Automotive Mechanical Design Process');
#17165=PRODUCT_CONTEXT('part definition',#17164,'mechanical');
#17213=PRODUCT('Horizontal link pin (1)','Horizontal link pin (1)',
'Horizontal link pin (1)',(#17165));
#17285=COLOUR_RGB('Grey',0.48,0.52,0.57);
#17286=FILL_AREA_STYLE_COLOUR('',#17285);
#17287=FILL_AREA_STYLE('',(#17286));
#17288=SURFACE_STYLE_FILL_AREA(#17287);
#17289=SURFACE_SIDE_STYLE('',(#17288));
#17290=SURFACE_STYLE_USAGE(.BOTH.,#17289);
#17291=PRESENTATION_STYLE_ASSIGNMENT((#17290));
ENDSEC;
END-ISO-10303-21;
